ISO-10303-21;
HEADER;
/* Generated by software containing ST-Developer
 * from STEP Tools, Inc. (www.steptools.com) 
 */

FILE_DESCRIPTION(
/* description */ ('Counterbalanced vertical column'),
/* implementation_level */ '2;1');

FILE_NAME(
/* name */ 'M10 rod nut.step',
/* time_stamp */ '2026-10-29T16:47:22-07:00',
/* author */ (''),
/* organization */ (''),
/* preprocessor_version */ 'ST-DEVELOPER v20.2',
/* originating_system */ 'Autodesk Translation Framework v15.17.0.0',
/* authorisation */ '');

FILE_SCHEMA (('AUTOMOTIVE_DESIGN { 1 0 10303 214 3 1 1 }'));
ENDSEC;

DATA;
#10=MECHANICAL_DESIGN_GEOMETRIC_PRESENTATION_REPRESENTATION('',(#376),#15040);
#306=SHAPE_REPRESENTATION_RELATIONSHIP('SRR','None',#15211,#341);
#341=ADVANCED_BREP_SHAPE_REPRESENTATION('',(#409),#15030);
#376=STYLED_ITEM('',(#15464),#409);
#409=MANIFOLD_SOLID_BREP('Body1',#7101);
#519=FACE_BOUND('',#1643,.T.);
#520=FACE_BOUND('',#1645,.T.);
#748=PLANE('',#8017);
#749=PLANE('',#8018);
#1132=FACE_OUTER_BOUND('',#1640,.T.);
#1133=FACE_OUTER_BOUND('',#1641,.T.);
#1134=FACE_OUTER_BOUND('',#1642,.T.);
#1135=FACE_OUTER_BOUND('',#1644,.T.);
#1640=EDGE_LOOP('',(#6126,#6127,#6128,#6129));
#1641=EDGE_LOOP('',(#6130,#6131,#6132,#6133));
#1642=EDGE_LOOP('',(#6134));
#1643=EDGE_LOOP('',(#6135));
#1644=EDGE_LOOP('',(#6136));
#1645=EDGE_LOOP('',(#6137));
#2241=LINE('',#14427,#2912);
#2242=LINE('',#14433,#2913);
#2912=VECTOR('',#9741,0.425);
#2913=VECTOR('',#9748,0.9);
#3263=CIRCLE('',#8012,0.425);
#3264=CIRCLE('',#8013,0.425);
#3265=CIRCLE('',#8015,0.9);
#3266=CIRCLE('',#8016,0.9);
#3748=VERTEX_POINT('',#14424);
#3749=VERTEX_POINT('',#14426);
#3750=VERTEX_POINT('',#14430);
#3751=VERTEX_POINT('',#14432);
#4564=EDGE_CURVE('',#3748,#3748,#3263,.T.);
#4565=EDGE_CURVE('',#3748,#3749,#2241,.T.);
#4566=EDGE_CURVE('',#3749,#3749,#3264,.T.);
#4567=EDGE_CURVE('',#3750,#3750,#3265,.T.);
#4568=EDGE_CURVE('',#3750,#3751,#2242,.T.);
#4569=EDGE_CURVE('',#3751,#3751,#3266,.T.);
#6126=ORIENTED_EDGE('',*,*,#4564,.F.);
#6127=ORIENTED_EDGE('',*,*,#4565,.T.);
#6128=ORIENTED_EDGE('',*,*,#4566,.T.);
#6129=ORIENTED_EDGE('',*,*,#4565,.F.);
#6130=ORIENTED_EDGE('',*,*,#4567,.F.);
#6131=ORIENTED_EDGE('',*,*,#4568,.T.);
#6132=ORIENTED_EDGE('',*,*,#4569,.T.);
#6133=ORIENTED_EDGE('',*,*,#4568,.F.);
#6134=ORIENTED_EDGE('',*,*,#4567,.T.);
#6135=ORIENTED_EDGE('',*,*,#4564,.T.);
#6136=ORIENTED_EDGE('',*,*,#4569,.F.);
#6137=ORIENTED_EDGE('',*,*,#4566,.F.);
#6654=CYLINDRICAL_SURFACE('',#8011,0.425);
#6655=CYLINDRICAL_SURFACE('',#8014,0.9);
#6974=ADVANCED_FACE('',(#1132),#6654,.F.);
#6975=ADVANCED_FACE('',(#1133),#6655,.T.);
#6976=ADVANCED_FACE('',(#1134,#519),#748,.T.);
#6977=ADVANCED_FACE('',(#1135,#520),#749,.F.);
#7101=CLOSED_SHELL('',(#6974,#6975,#6976,#6977));
#8010=AXIS2_PLACEMENT_3D('',#14422,#9735,#9736);
#8011=AXIS2_PLACEMENT_3D('',#14423,#9737,#9738);
#8012=AXIS2_PLACEMENT_3D('',#14425,#9739,#9740);
#8013=AXIS2_PLACEMENT_3D('',#14428,#9742,#9743);
#8014=AXIS2_PLACEMENT_3D('',#14429,#9744,#9745);
#8015=AXIS2_PLACEMENT_3D('',#14431,#9746,#9747);
#8016=AXIS2_PLACEMENT_3D('',#14434,#9749,#9750);
#8017=AXIS2_PLACEMENT_3D('',#14435,#9751,#9752);
#8018=AXIS2_PLACEMENT_3D('',#14436,#9753,#9754);
#9735=DIRECTION('axis',(0.,0.,1.));
#9736=DIRECTION('refdir',(1.,0.,0.));
#9737=DIRECTION('center_axis',(0.,0.,1.));
#9738=DIRECTION('ref_axis',(1.,0.,0.));
#9739=DIRECTION('center_axis',(0.,0.,-1.));
#9740=DIRECTION('ref_axis',(1.,0.,0.));
#9741=DIRECTION('',(0.,0.,-1.));
#9742=DIRECTION('center_axis',(0.,0.,-1.));
#9743=DIRECTION('ref_axis',(1.,0.,0.));
#9744=DIRECTION('center_axis',(0.,0.,1.));
#9745=DIRECTION('ref_axis',(1.,0.,0.));
#9746=DIRECTION('center_axis',(0.,0.,1.));
#9747=DIRECTION('ref_axis',(1.,0.,0.));
#9748=DIRECTION('',(0.,0.,-1.));
#9749=DIRECTION('center_axis',(0.,0.,1.));
#9750=DIRECTION('ref_axis',(1.,0.,0.));
#9751=DIRECTION('center_axis',(0.,0.,1.));
#9752=DIRECTION('ref_axis',(1.,0.,0.));
#9753=DIRECTION('center_axis',(0.,0.,1.));
#9754=DIRECTION('ref_axis',(1.,0.,0.));
#14422=CARTESIAN_POINT('',(0.,0.,0.));
#14423=CARTESIAN_POINT('Origin',(-7.,0.,22.));
#14424=CARTESIAN_POINT('',(-7.425,-5.20474889637625E-17,22.8));
#14425=CARTESIAN_POINT('Origin',(-7.,0.,22.8));
#14426=CARTESIAN_POINT('',(-7.425,-5.20474889637625E-17,22.));
#14427=CARTESIAN_POINT('',(-7.425,-5.20474889637625E-17,22.));
#14428=CARTESIAN_POINT('Origin',(-7.,0.,22.));
#14429=CARTESIAN_POINT('Origin',(-7.,0.,22.));
#14430=CARTESIAN_POINT('',(-7.9,-1.10218211923262E-16,22.8));
#14431=CARTESIAN_POINT('Origin',(-7.,0.,22.8));
#14432=CARTESIAN_POINT('',(-7.9,-1.10218211923262E-16,22.));
#14433=CARTESIAN_POINT('',(-7.9,-1.10218211923262E-16,22.));
#14434=CARTESIAN_POINT('Origin',(-7.,0.,22.));
#14435=CARTESIAN_POINT('Origin',(-7.,0.,22.8));
#14436=CARTESIAN_POINT('Origin',(-7.,0.,22.));
#14990=UNCERTAINTY_MEASURE_WITH_UNIT(LENGTH_MEASURE(0.001),#15041,
'DISTANCE_ACCURACY_VALUE',
'Maximum model space distance between geometric entities at asserted c
onnectivities');
#15000=UNCERTAINTY_MEASURE_WITH_UNIT(LENGTH_MEASURE(0.001),#15041,
'DISTANCE_ACCURACY_VALUE',
'Maximum model space distance between geometric entities at asserted c
onnectivities');
#15030=(
GEOMETRIC_REPRESENTATION_CONTEXT(3)
GLOBAL_UNCERTAINTY_ASSIGNED_CONTEXT((#14990))
GLOBAL_UNIT_ASSIGNED_CONTEXT((#15041,#15043,#15044))
REPRESENTATION_CONTEXT('','3D')
);
#15040=(
GEOMETRIC_REPRESENTATION_CONTEXT(3)
GLOBAL_UNCERTAINTY_ASSIGNED_CONTEXT((#15000))
GLOBAL_UNIT_ASSIGNED_CONTEXT((#15041,#15043,#15044))
REPRESENTATION_CONTEXT('','3D')
);
#15041=(
LENGTH_UNIT()
NAMED_UNIT(*)
SI_UNIT(.CENTI.,.METRE.)
);
#15043=(
NAMED_UNIT(*)
PLANE_ANGLE_UNIT()
SI_UNIT($,.RADIAN.)
);
#15044=(
NAMED_UNIT(*)
SI_UNIT($,.STERADIAN.)
SOLID_ANGLE_UNIT()
);
#15074=SHAPE_DEFINITION_REPRESENTATION(#15113,#15211);
#15113=PRODUCT_DEFINITION_SHAPE('',$,#15251);
#15211=SHAPE_REPRESENTATION('',(#8010),#15030);
#15221=PRODUCT_DEFINITION_CONTEXT('part definition',#15340,'design');
#15251=PRODUCT_DEFINITION('M10 rod nut','M10 rod nut',#15290,#15221);
#15290=PRODUCT_DEFINITION_FORMATION('',$,#15371);
#15340=APPLICATION_CONTEXT(
'Core Data for Automotive Mechanical Design Process');
#15341=PRODUCT_CONTEXT('part definition',#15340,'mechanical');
#15371=PRODUCT('M10 rod nut','M10 rod nut','M10 rod nut',(#15341));
#15458=COLOUR_RGB('Black',0.12,0.14,0.17);
#15459=FILL_AREA_STYLE_COLOUR('',#15458);
#15460=FILL_AREA_STYLE('',(#15459));
#15461=SURFACE_STYLE_FILL_AREA(#15460);
#15462=SURFACE_SIDE_STYLE('',(#15461));
#15463=SURFACE_STYLE_USAGE(.BOTH.,#15462);
#15464=PRESENTATION_STYLE_ASSIGNMENT((#15463));
ENDSEC;
END-ISO-10303-21;
